ISO-10303-21;
HEADER;
/* Generated by software containing ST-Developer
 * from STEP Tools, Inc. (www.steptools.com) 
 */

FILE_DESCRIPTION(
/* description */ (''),
/* implementation_level */ '2;1');

FILE_NAME(
/* name */ '07_ISO_7089_Washer_10.step',
/* time_stamp */ '2026-10-11T08:27:52-07:00',
/* author */ (''),
/* organization */ (''),
/* preprocessor_version */ 'ST-DEVELOPER v20.2',
/* originating_system */ 'Autodesk Translation Framework v15.15.0.0',
/* authorisation */ '');

FILE_SCHEMA (('AUTOMOTIVE_DESIGN { 1 0 10303 214 3 1 1 }'));
ENDSEC;

DATA;
#10=MECHANICAL_DESIGN_GEOMETRIC_PRESENTATION_REPRESENTATION('',(#925),#94301);
#897=SHAPE_REPRESENTATION_RELATIONSHIP('SRR','None',#94377,#911);
#911=ADVANCED_BREP_SHAPE_REPRESENTATION('',(#939),#94293);
#925=STYLED_ITEM('',(#94588),#939);
#939=MANIFOLD_SOLID_BREP('Body1',#51024);
#1033=FACE_BOUND('',#18371,.T.);
#1034=FACE_BOUND('',#18376,.T.);
#1192=CYLINDRICAL_SURFACE('',#54816,10.);
#1193=CYLINDRICAL_SURFACE('',#54824,5.25);
#6285=LINE('',#87371,#10813);
#6286=LINE('',#87376,#10814);
#6287=LINE('',#87380,#10815);
#6288=LINE('',#87386,#10816);
#6289=LINE('',#87390,#10817);
#6290=LINE('',#87394,#10818);
#10813=VECTOR('',#66749,9.9);
#10814=VECTOR('',#66756,10.);
#10815=VECTOR('',#66761,9.9);
#10816=VECTOR('',#66768,5.35);
#10817=VECTOR('',#66773,5.25);
#10818=VECTOR('',#66778,5.35);
#13059=PLANE('',#54820);
#13060=PLANE('',#54828);
#15611=FACE_OUTER_BOUND('',#18367,.T.);
#15612=FACE_OUTER_BOUND('',#18368,.T.);
#15613=FACE_OUTER_BOUND('',#18369,.T.);
#15614=FACE_OUTER_BOUND('',#18370,.T.);
#15615=FACE_OUTER_BOUND('',#18372,.T.);
#15616=FACE_OUTER_BOUND('',#18373,.T.);
#15617=FACE_OUTER_BOUND('',#18374,.T.);
#15618=FACE_OUTER_BOUND('',#18375,.T.);
#18367=EDGE_LOOP('',(#46507,#46508,#46509,#46510));
#18368=EDGE_LOOP('',(#46511,#46512,#46513,#46514));
#18369=EDGE_LOOP('',(#46515,#46516,#46517,#46518));
#18370=EDGE_LOOP('',(#46519));
#18371=EDGE_LOOP('',(#46520));
#18372=EDGE_LOOP('',(#46521,#46522,#46523,#46524));
#18373=EDGE_LOOP('',(#46525,#46526,#46527,#46528));
#18374=EDGE_LOOP('',(#46529,#46530,#46531,#46532));
#18375=EDGE_LOOP('',(#46533));
#18376=EDGE_LOOP('',(#46534));
#20134=CIRCLE('',#54814,10.);
#20135=CIRCLE('',#54815,9.8);
#20136=CIRCLE('',#54817,10.);
#20137=CIRCLE('',#54819,9.8);
#20138=CIRCLE('',#54821,5.45);
#20139=CIRCLE('',#54823,5.25);
#20140=CIRCLE('',#54825,5.25);
#20141=CIRCLE('',#54827,5.45);
#24816=VERTEX_POINT('',#87368);
#24817=VERTEX_POINT('',#87370);
#24818=VERTEX_POINT('',#87374);
#24819=VERTEX_POINT('',#87378);
#24820=VERTEX_POINT('',#87382);
#24821=VERTEX_POINT('',#87385);
#24822=VERTEX_POINT('',#87389);
#24823=VERTEX_POINT('',#87393);
#32115=EDGE_CURVE('',#24816,#24816,#20134,.T.);
#32116=EDGE_CURVE('',#24816,#24817,#6285,.T.);
#32117=EDGE_CURVE('',#24817,#24817,#20135,.T.);
#32118=EDGE_CURVE('',#24818,#24818,#20136,.T.);
#32119=EDGE_CURVE('',#24818,#24816,#6286,.T.);
#32120=EDGE_CURVE('',#24819,#24819,#20137,.T.);
#32121=EDGE_CURVE('',#24819,#24818,#6287,.T.);
#32122=EDGE_CURVE('',#24820,#24820,#20138,.T.);
#32123=EDGE_CURVE('',#24820,#24821,#6288,.T.);
#32124=EDGE_CURVE('',#24821,#24821,#20139,.T.);
#32125=EDGE_CURVE('',#24821,#24822,#6289,.T.);
#32126=EDGE_CURVE('',#24822,#24822,#20140,.T.);
#32127=EDGE_CURVE('',#24822,#24823,#6290,.T.);
#32128=EDGE_CURVE('',#24823,#24823,#20141,.T.);
#46507=ORIENTED_EDGE('',*,*,#32115,.F.);
#46508=ORIENTED_EDGE('',*,*,#32116,.T.);
#46509=ORIENTED_EDGE('',*,*,#32117,.T.);
#46510=ORIENTED_EDGE('',*,*,#32116,.F.);
#46511=ORIENTED_EDGE('',*,*,#32118,.F.);
#46512=ORIENTED_EDGE('',*,*,#32119,.T.);
#46513=ORIENTED_EDGE('',*,*,#32115,.T.);
#46514=ORIENTED_EDGE('',*,*,#32119,.F.);
#46515=ORIENTED_EDGE('',*,*,#32120,.F.);
#46516=ORIENTED_EDGE('',*,*,#32121,.T.);
#46517=ORIENTED_EDGE('',*,*,#32118,.T.);
#46518=ORIENTED_EDGE('',*,*,#32121,.F.);
#46519=ORIENTED_EDGE('',*,*,#32120,.T.);
#46520=ORIENTED_EDGE('',*,*,#32122,.F.);
#46521=ORIENTED_EDGE('',*,*,#32122,.T.);
#46522=ORIENTED_EDGE('',*,*,#32123,.T.);
#46523=ORIENTED_EDGE('',*,*,#32124,.F.);
#46524=ORIENTED_EDGE('',*,*,#32123,.F.);
#46525=ORIENTED_EDGE('',*,*,#32124,.T.);
#46526=ORIENTED_EDGE('',*,*,#32125,.T.);
#46527=ORIENTED_EDGE('',*,*,#32126,.F.);
#46528=ORIENTED_EDGE('',*,*,#32125,.F.);
#46529=ORIENTED_EDGE('',*,*,#32126,.T.);
#46530=ORIENTED_EDGE('',*,*,#32127,.T.);
#46531=ORIENTED_EDGE('',*,*,#32128,.F.);
#46532=ORIENTED_EDGE('',*,*,#32127,.F.);
#46533=ORIENTED_EDGE('',*,*,#32117,.F.);
#46534=ORIENTED_EDGE('',*,*,#32128,.T.);
#48309=CONICAL_SURFACE('',#54813,9.9,0.785398163397446);
#48310=CONICAL_SURFACE('',#54818,9.9,0.785398163397446);
#48311=CONICAL_SURFACE('',#54822,5.35,0.785398163397448);
#48312=CONICAL_SURFACE('',#54826,5.35,0.785398163397449);
#50698=ADVANCED_FACE('',(#15611),#48309,.T.);
#50699=ADVANCED_FACE('',(#15612),#1192,.T.);
#50700=ADVANCED_FACE('',(#15613),#48310,.T.);
#50701=ADVANCED_FACE('',(#15614,#1033),#13059,.T.);
#50702=ADVANCED_FACE('',(#15615),#48311,.F.);
#50703=ADVANCED_FACE('',(#15616),#1193,.F.);
#50704=ADVANCED_FACE('',(#15617),#48312,.F.);
#50705=ADVANCED_FACE('',(#15618,#1034),#13060,.T.);
#51024=CLOSED_SHELL('',(#50698,#50699,#50700,#50701,#50702,#50703,#50704,
#50705));
#54812=AXIS2_PLACEMENT_3D('',#87366,#66743,#66744);
#54813=AXIS2_PLACEMENT_3D('',#87367,#66745,#66746);
#54814=AXIS2_PLACEMENT_3D('',#87369,#66747,#66748);
#54815=AXIS2_PLACEMENT_3D('',#87372,#66750,#66751);
#54816=AXIS2_PLACEMENT_3D('',#87373,#66752,#66753);
#54817=AXIS2_PLACEMENT_3D('',#87375,#66754,#66755);
#54818=AXIS2_PLACEMENT_3D('',#87377,#66757,#66758);
#54819=AXIS2_PLACEMENT_3D('',#87379,#66759,#66760);
#54820=AXIS2_PLACEMENT_3D('',#87381,#66762,#66763);
#54821=AXIS2_PLACEMENT_3D('',#87383,#66764,#66765);
#54822=AXIS2_PLACEMENT_3D('',#87384,#66766,#66767);
#54823=AXIS2_PLACEMENT_3D('',#87387,#66769,#66770);
#54824=AXIS2_PLACEMENT_3D('',#87388,#66771,#66772);
#54825=AXIS2_PLACEMENT_3D('',#87391,#66774,#66775);
#54826=AXIS2_PLACEMENT_3D('',#87392,#66776,#66777);
#54827=AXIS2_PLACEMENT_3D('',#87395,#66779,#66780);
#54828=AXIS2_PLACEMENT_3D('',#87396,#66781,#66782);
#66743=DIRECTION('axis',(0.,0.,1.));
#66744=DIRECTION('refdir',(1.,0.,0.));
#66745=DIRECTION('center_axis',(1.,0.,0.));
#66746=DIRECTION('ref_axis',(0.,1.,0.));
#66747=DIRECTION('center_axis',(1.,0.,0.));
#66748=DIRECTION('ref_axis',(0.,0.,-1.));
#66749=DIRECTION('',(-0.707106781186549,0.707106781186546,8.65956056235492E-17));
#66750=DIRECTION('center_axis',(1.,0.,0.));
#66751=DIRECTION('ref_axis',(0.,0.,-1.));
#66752=DIRECTION('center_axis',(1.,0.,0.));
#66753=DIRECTION('ref_axis',(0.,1.,0.));
#66754=DIRECTION('center_axis',(1.,0.,0.));
#66755=DIRECTION('ref_axis',(0.,0.,-1.));
#66756=DIRECTION('',(-1.,0.,0.));
#66757=DIRECTION('center_axis',(-1.,0.,0.));
#66758=DIRECTION('ref_axis',(0.,1.,0.));
#66759=DIRECTION('center_axis',(1.,0.,0.));
#66760=DIRECTION('ref_axis',(0.,0.,-1.));
#66761=DIRECTION('',(-0.707106781186549,-0.707106781186545,-8.65956056235491E-17));
#66762=DIRECTION('center_axis',(1.,0.,0.));
#66763=DIRECTION('ref_axis',(0.,0.,-1.));
#66764=DIRECTION('center_axis',(1.,0.,0.));
#66765=DIRECTION('ref_axis',(0.,0.,-1.));
#66766=DIRECTION('center_axis',(1.,0.,0.));
#66767=DIRECTION('ref_axis',(0.,1.,0.));
#66768=DIRECTION('',(-0.707106781186548,0.707106781186548,8.65956056235493E-17));
#66769=DIRECTION('center_axis',(1.,0.,0.));
#66770=DIRECTION('ref_axis',(0.,0.,-1.));
#66771=DIRECTION('center_axis',(1.,0.,0.));
#66772=DIRECTION('ref_axis',(0.,1.,0.));
#66773=DIRECTION('',(-1.,0.,0.));
#66774=DIRECTION('center_axis',(1.,0.,0.));
#66775=DIRECTION('ref_axis',(0.,0.,-1.));
#66776=DIRECTION('center_axis',(-1.,0.,0.));
#66777=DIRECTION('ref_axis',(0.,1.,0.));
#66778=DIRECTION('',(-0.707106781186547,-0.707106781186548,-8.65956056235494E-17));
#66779=DIRECTION('center_axis',(1.,0.,0.));
#66780=DIRECTION('ref_axis',(0.,0.,-1.));
#66781=DIRECTION('center_axis',(-1.,0.,0.));
#66782=DIRECTION('ref_axis',(0.,0.,1.));
#87366=CARTESIAN_POINT('',(0.,0.,0.));
#87367=CARTESIAN_POINT('Origin',(0.1,0.,0.));
#87368=CARTESIAN_POINT('',(0.2,-10.,-1.22464679914735E-15));
#87369=CARTESIAN_POINT('Origin',(0.2,0.,0.));
#87370=CARTESIAN_POINT('',(1.21430643318376E-16,-9.8,-1.20015386316441E-15));
#87371=CARTESIAN_POINT('',(0.1,-9.9,-1.21240033115588E-15));
#87372=CARTESIAN_POINT('Origin',(0.,0.,0.));
#87373=CARTESIAN_POINT('Origin',(1.,0.,0.));
#87374=CARTESIAN_POINT('',(1.8,-10.,-1.22464679914735E-15));
#87375=CARTESIAN_POINT('Origin',(1.8,0.,0.));
#87376=CARTESIAN_POINT('',(1.,-10.,-1.22464679914735E-15));
#87377=CARTESIAN_POINT('Origin',(1.9,0.,0.));
#87378=CARTESIAN_POINT('',(2.,-9.8,-1.20015386316441E-15));
#87379=CARTESIAN_POINT('Origin',(2.,0.,0.));
#87380=CARTESIAN_POINT('',(1.9,-9.9,-1.21240033115588E-15));
#87381=CARTESIAN_POINT('Origin',(2.,5.45,0.));
#87382=CARTESIAN_POINT('',(2.,-5.45,-6.67432505535308E-16));
#87383=CARTESIAN_POINT('Origin',(2.,0.,0.));
#87384=CARTESIAN_POINT('Origin',(1.9,0.,0.));
#87385=CARTESIAN_POINT('',(1.8,-5.25,-6.42939569552361E-16));
#87386=CARTESIAN_POINT('',(1.9,-5.35,-6.55186037543834E-16));
#87387=CARTESIAN_POINT('Origin',(1.8,0.,0.));
#87388=CARTESIAN_POINT('Origin',(1.,0.,0.));
#87389=CARTESIAN_POINT('',(0.2,-5.25,-6.42939569552361E-16));
#87390=CARTESIAN_POINT('',(1.,-5.25,-6.42939569552361E-16));
#87391=CARTESIAN_POINT('Origin',(0.2,0.,0.));
#87392=CARTESIAN_POINT('Origin',(0.1,0.,0.));
#87393=CARTESIAN_POINT('',(-8.67361737988404E-17,-5.45,-6.67432505535308E-16));
#87394=CARTESIAN_POINT('',(0.1,-5.35,-6.55186037543834E-16));
#87395=CARTESIAN_POINT('Origin',(0.,0.,0.));
#87396=CARTESIAN_POINT('Origin',(0.,9.8,0.));
#94277=UNCERTAINTY_MEASURE_WITH_UNIT(LENGTH_MEASURE(0.01),#94302,
'DISTANCE_ACCURACY_VALUE',
'Maximum model space distance between geometric entities at asserted c
onnectivities');
#94285=UNCERTAINTY_MEASURE_WITH_UNIT(LENGTH_MEASURE(0.01),#94302,
'DISTANCE_ACCURACY_VALUE',
'Maximum model space distance between geometric entities at asserted c
onnectivities');
#94293=(
GEOMETRIC_REPRESENTATION_CONTEXT(3)
GLOBAL_UNCERTAINTY_ASSIGNED_CONTEXT((#94277))
GLOBAL_UNIT_ASSIGNED_CONTEXT((#94302,#94304,#94305))
REPRESENTATION_CONTEXT('','3D')
);
#94301=(
GEOMETRIC_REPRESENTATION_CONTEXT(3)
GLOBAL_UNCERTAINTY_ASSIGNED_CONTEXT((#94285))
GLOBAL_UNIT_ASSIGNED_CONTEXT((#94302,#94304,#94305))
REPRESENTATION_CONTEXT('','3D')
);
#94302=(
LENGTH_UNIT()
NAMED_UNIT(*)
SI_UNIT(.MILLI.,.METRE.)
);
#94304=(
NAMED_UNIT(*)
PLANE_ANGLE_UNIT()
SI_UNIT($,.RADIAN.)
);
#94305=(
NAMED_UNIT(*)
SI_UNIT($,.STERADIAN.)
SOLID_ANGLE_UNIT()
);
#94313=SHAPE_DEFINITION_REPRESENTATION(#94328,#94377);
#94328=PRODUCT_DEFINITION_SHAPE('',$,#94393);
#94377=SHAPE_REPRESENTATION('',(#54812),#94293);
#94385=PRODUCT_DEFINITION_CONTEXT('part definition',#94432,'design');
#94393=PRODUCT_DEFINITION('2026-10-11-08-26-40-364',
'07_ISO_7089_Washer_10',#94408,#94385);
#94408=PRODUCT_DEFINITION_FORMATION('',$,#94441);
#94432=APPLICATION_CONTEXT(
'Core Data for Automotive Mechanical Design Process');
#94433=PRODUCT_CONTEXT('part definition',#94432,'mechanical');
#94441=PRODUCT('2026-10-11-08-26-40-364','07_ISO_7089_Washer_10',$,(#94433));
#94582=COLOUR_RGB('Black',0.12,0.14,0.17);
#94583=FILL_AREA_STYLE_COLOUR('',#94582);
#94584=FILL_AREA_STYLE('',(#94583));
#94585=SURFACE_STYLE_FILL_AREA(#94584);
#94586=SURFACE_SIDE_STYLE('',(#94585));
#94587=SURFACE_STYLE_USAGE(.BOTH.,#94586);
#94588=PRESENTATION_STYLE_ASSIGNMENT((#94587));
ENDSEC;
END-ISO-10303-21;
